ISO-10303-21;
HEADER;
/* Generated by software containing ST-Developer
 * from STEP Tools, Inc. (www.steptools.com) 
 */

FILE_DESCRIPTION(
/* description */ ('Telescoping shaft support with lock collar'),
/* implementation_level */ '2;1');

FILE_NAME(
/* name */ 'Cap Screw - M4x16.step',
/* time_stamp */ '2026-10-27T10:48:51-07:00',
/* author */ (''),
/* organization */ (''),
/* preprocessor_version */ 'ST-DEVELOPER v20.2',
/* originating_system */ 'Autodesk Translation Framework v15.17.0.0',
/* authorisation */ '');

FILE_SCHEMA (('AUTOMOTIVE_DESIGN { 1 0 10303 214 3 1 1 }'));
ENDSEC;

DATA;
#10=MECHANICAL_DESIGN_GEOMETRIC_PRESENTATION_REPRESENTATION('',(#260),#7349);
#168=ORIENTED_CLOSED_SHELL('',*,#3985,.F.);
#177=CONICAL_SURFACE('',#4647,0.325,0.785398163397448);
#178=CONICAL_SURFACE('',#4651,0.335,0.785398163397448);
#179=CONICAL_SURFACE('',#4655,0.21,0.463647609000806);
#180=CONICAL_SURFACE('',#4659,0.18,0.785398163397448);
#182=BREP_WITH_VOIDS('Body1',#3984,(#168));
#220=SHAPE_REPRESENTATION_RELATIONSHIP('SRR','None',#7464,#240);
#240=ADVANCED_BREP_SHAPE_REPRESENTATION('',(#182),#7348);
#260=STYLED_ITEM('',(#7634),#182);
#358=FACE_BOUND('',#1014,.T.);
#484=PLANE('',#4645);
#485=PLANE('',#4653);
#486=PLANE('',#4661);
#487=PLANE('',#4662);
#488=PLANE('',#4663);
#489=PLANE('',#4664);
#490=PLANE('',#4665);
#491=PLANE('',#4666);
#492=PLANE('',#4667);
#493=PLANE('',#4668);
#494=PLANE('',#4669);
#704=FACE_OUTER_BOUND('',#1009,.T.);
#705=FACE_OUTER_BOUND('',#1010,.T.);
#706=FACE_OUTER_BOUND('',#1011,.T.);
#707=FACE_OUTER_BOUND('',#1012,.T.);
#708=FACE_OUTER_BOUND('',#1013,.T.);
#709=FACE_OUTER_BOUND('',#1015,.T.);
#710=FACE_OUTER_BOUND('',#1016,.T.);
#711=FACE_OUTER_BOUND('',#1017,.T.);
#712=FACE_OUTER_BOUND('',#1018,.T.);
#713=FACE_OUTER_BOUND('',#1019,.T.);
#714=FACE_OUTER_BOUND('',#1020,.T.);
#715=FACE_OUTER_BOUND('',#1021,.T.);
#716=FACE_OUTER_BOUND('',#1022,.T.);
#717=FACE_OUTER_BOUND('',#1023,.T.);
#718=FACE_OUTER_BOUND('',#1024,.T.);
#719=FACE_OUTER_BOUND('',#1025,.T.);
#720=FACE_OUTER_BOUND('',#1026,.T.);
#1009=EDGE_LOOP('',(#3596));
#1010=EDGE_LOOP('',(#3597,#3598,#3599,#3600));
#1011=EDGE_LOOP('',(#3601,#3602,#3603,#3604));
#1012=EDGE_LOOP('',(#3605,#3606,#3607,#3608));
#1013=EDGE_LOOP('',(#3609));
#1014=EDGE_LOOP('',(#3610));
#1015=EDGE_LOOP('',(#3611,#3612,#3613,#3614));
#1016=EDGE_LOOP('',(#3615,#3616,#3617,#3618));
#1017=EDGE_LOOP('',(#3619,#3620,#3621,#3622));
#1018=EDGE_LOOP('',(#3623));
#1019=EDGE_LOOP('',(#3624,#3625,#3626,#3627));
#1020=EDGE_LOOP('',(#3628,#3629,#3630,#3631));
#1021=EDGE_LOOP('',(#3632,#3633,#3634,#3635));
#1022=EDGE_LOOP('',(#3636,#3637,#3638,#3639));
#1023=EDGE_LOOP('',(#3640,#3641,#3642,#3643));
#1024=EDGE_LOOP('',(#3644,#3645,#3646,#3647));
#1025=EDGE_LOOP('',(#3648,#3649,#3650,#3651,#3652,#3653));
#1026=EDGE_LOOP('',(#3654,#3655,#3656,#3657,#3658,#3659));
#1283=LINE('',#7200,#1563);
#1284=LINE('',#7204,#1564);
#1285=LINE('',#7208,#1565);
#1286=LINE('',#7215,#1566);
#1287=LINE('',#7219,#1567);
#1288=LINE('',#7223,#1568);
#1289=LINE('',#7228,#1569);
#1290=LINE('',#7230,#1570);
#1291=LINE('',#7232,#1571);
#1292=LINE('',#7233,#1572);
#1293=LINE('',#7236,#1573);
#1294=LINE('',#7238,#1574);
#1295=LINE('',#7239,#1575);
#1296=LINE('',#7242,#1576);
#1297=LINE('',#7244,#1577);
#1298=LINE('',#7245,#1578);
#1299=LINE('',#7248,#1579);
#1300=LINE('',#7250,#1580);
#1301=LINE('',#7251,#1581);
#1302=LINE('',#7254,#1582);
#1303=LINE('',#7256,#1583);
#1304=LINE('',#7257,#1584);
#1305=LINE('',#7259,#1585);
#1306=LINE('',#7260,#1586);
#1563=VECTOR('',#5847,0.325);
#1564=VECTOR('',#5852,0.35);
#1565=VECTOR('',#5857,0.335);
#1566=VECTOR('',#5866,0.21);
#1567=VECTOR('',#5871,0.2);
#1568=VECTOR('',#5876,0.18);
#1569=VECTOR('',#5881,1.);
#1570=VECTOR('',#5882,1.);
#1571=VECTOR('',#5883,1.);
#1572=VECTOR('',#5884,1.);
#1573=VECTOR('',#5887,1.);
#1574=VECTOR('',#5888,1.);
#1575=VECTOR('',#5889,1.);
#1576=VECTOR('',#5892,1.);
#1577=VECTOR('',#5893,1.);
#1578=VECTOR('',#5894,1.);
#1579=VECTOR('',#5897,1.);
#1580=VECTOR('',#5898,1.);
#1581=VECTOR('',#5899,1.);
#1582=VECTOR('',#5902,1.);
#1583=VECTOR('',#5903,1.);
#1584=VECTOR('',#5904,1.);
#1585=VECTOR('',#5907,1.);
#1586=VECTOR('',#5908,1.);
#1790=CIRCLE('',#4646,0.3);
#1791=CIRCLE('',#4648,0.35);
#1792=CIRCLE('',#4650,0.35);
#1793=CIRCLE('',#4652,0.32);
#1794=CIRCLE('',#4654,0.22);
#1795=CIRCLE('',#4656,0.1954);
#1796=CIRCLE('',#4658,0.1954);
#1797=CIRCLE('',#4660,0.16);
#2113=VERTEX_POINT('',#7195);
#2114=VERTEX_POINT('',#7198);
#2115=VERTEX_POINT('',#7202);
#2116=VERTEX_POINT('',#7206);
#2117=VERTEX_POINT('',#7210);
#2118=VERTEX_POINT('',#7213);
#2119=VERTEX_POINT('',#7217);
#2120=VERTEX_POINT('',#7221);
#2121=VERTEX_POINT('',#7226);
#2122=VERTEX_POINT('',#7227);
#2123=VERTEX_POINT('',#7229);
#2124=VERTEX_POINT('',#7231);
#2125=VERTEX_POINT('',#7235);
#2126=VERTEX_POINT('',#7237);
#2127=VERTEX_POINT('',#7241);
#2128=VERTEX_POINT('',#7243);
#2129=VERTEX_POINT('',#7247);
#2130=VERTEX_POINT('',#7249);
#2131=VERTEX_POINT('',#7253);
#2132=VERTEX_POINT('',#7255);
#2610=EDGE_CURVE('',#2113,#2113,#1790,.T.);
#2611=EDGE_CURVE('',#2114,#2114,#1791,.T.);
#2612=EDGE_CURVE('',#2114,#2113,#1283,.T.);
#2613=EDGE_CURVE('',#2115,#2115,#1792,.T.);
#2614=EDGE_CURVE('',#2115,#2114,#1284,.T.);
#2615=EDGE_CURVE('',#2116,#2116,#1793,.T.);
#2616=EDGE_CURVE('',#2116,#2115,#1285,.T.);
#2617=EDGE_CURVE('',#2117,#2117,#1794,.T.);
#2618=EDGE_CURVE('',#2118,#2118,#1795,.F.);
#2619=EDGE_CURVE('',#2118,#2117,#1286,.T.);
#2620=EDGE_CURVE('',#2119,#2119,#1796,.F.);
#2621=EDGE_CURVE('',#2119,#2118,#1287,.T.);
#2622=EDGE_CURVE('',#2120,#2120,#1797,.T.);
#2623=EDGE_CURVE('',#2120,#2119,#1288,.T.);
#2624=EDGE_CURVE('',#2121,#2122,#1289,.T.);
#2625=EDGE_CURVE('',#2122,#2123,#1290,.T.);
#2626=EDGE_CURVE('',#2123,#2124,#1291,.T.);
#2627=EDGE_CURVE('',#2121,#2124,#1292,.T.);
#2628=EDGE_CURVE('',#2122,#2125,#1293,.T.);
#2629=EDGE_CURVE('',#2125,#2126,#1294,.T.);
#2630=EDGE_CURVE('',#2126,#2123,#1295,.T.);
#2631=EDGE_CURVE('',#2125,#2127,#1296,.T.);
#2632=EDGE_CURVE('',#2127,#2128,#1297,.T.);
#2633=EDGE_CURVE('',#2128,#2126,#1298,.T.);
#2634=EDGE_CURVE('',#2127,#2129,#1299,.T.);
#2635=EDGE_CURVE('',#2129,#2130,#1300,.T.);
#2636=EDGE_CURVE('',#2130,#2128,#1301,.T.);
#2637=EDGE_CURVE('',#2129,#2131,#1302,.T.);
#2638=EDGE_CURVE('',#2131,#2132,#1303,.T.);
#2639=EDGE_CURVE('',#2132,#2130,#1304,.T.);
#2640=EDGE_CURVE('',#2131,#2121,#1305,.T.);
#2641=EDGE_CURVE('',#2124,#2132,#1306,.T.);
#3596=ORIENTED_EDGE('',*,*,#2610,.F.);
#3597=ORIENTED_EDGE('',*,*,#2611,.F.);
#3598=ORIENTED_EDGE('',*,*,#2612,.T.);
#3599=ORIENTED_EDGE('',*,*,#2610,.T.);
#3600=ORIENTED_EDGE('',*,*,#2612,.F.);
#3601=ORIENTED_EDGE('',*,*,#2613,.F.);
#3602=ORIENTED_EDGE('',*,*,#2614,.T.);
#3603=ORIENTED_EDGE('',*,*,#2611,.T.);
#3604=ORIENTED_EDGE('',*,*,#2614,.F.);
#3605=ORIENTED_EDGE('',*,*,#2615,.F.);
#3606=ORIENTED_EDGE('',*,*,#2616,.T.);
#3607=ORIENTED_EDGE('',*,*,#2613,.T.);
#3608=ORIENTED_EDGE('',*,*,#2616,.F.);
#3609=ORIENTED_EDGE('',*,*,#2615,.T.);
#3610=ORIENTED_EDGE('',*,*,#2617,.F.);
#3611=ORIENTED_EDGE('',*,*,#2618,.F.);
#3612=ORIENTED_EDGE('',*,*,#2619,.T.);
#3613=ORIENTED_EDGE('',*,*,#2617,.T.);
#3614=ORIENTED_EDGE('',*,*,#2619,.F.);
#3615=ORIENTED_EDGE('',*,*,#2620,.F.);
#3616=ORIENTED_EDGE('',*,*,#2621,.T.);
#3617=ORIENTED_EDGE('',*,*,#2618,.T.);
#3618=ORIENTED_EDGE('',*,*,#2621,.F.);
#3619=ORIENTED_EDGE('',*,*,#2622,.F.);
#3620=ORIENTED_EDGE('',*,*,#2623,.T.);
#3621=ORIENTED_EDGE('',*,*,#2620,.T.);
#3622=ORIENTED_EDGE('',*,*,#2623,.F.);
#3623=ORIENTED_EDGE('',*,*,#2622,.T.);
#3624=ORIENTED_EDGE('',*,*,#2624,.T.);
#3625=ORIENTED_EDGE('',*,*,#2625,.T.);
#3626=ORIENTED_EDGE('',*,*,#2626,.T.);
#3627=ORIENTED_EDGE('',*,*,#2627,.F.);
#3628=ORIENTED_EDGE('',*,*,#2628,.T.);
#3629=ORIENTED_EDGE('',*,*,#2629,.T.);
#3630=ORIENTED_EDGE('',*,*,#2630,.T.);
#3631=ORIENTED_EDGE('',*,*,#2625,.F.);
#3632=ORIENTED_EDGE('',*,*,#2631,.T.);
#3633=ORIENTED_EDGE('',*,*,#2632,.T.);
#3634=ORIENTED_EDGE('',*,*,#2633,.T.);
#3635=ORIENTED_EDGE('',*,*,#2629,.F.);
#3636=ORIENTED_EDGE('',*,*,#2634,.T.);
#3637=ORIENTED_EDGE('',*,*,#2635,.T.);
#3638=ORIENTED_EDGE('',*,*,#2636,.T.);
#3639=ORIENTED_EDGE('',*,*,#2632,.F.);
#3640=ORIENTED_EDGE('',*,*,#2637,.T.);
#3641=ORIENTED_EDGE('',*,*,#2638,.T.);
#3642=ORIENTED_EDGE('',*,*,#2639,.T.);
#3643=ORIENTED_EDGE('',*,*,#2635,.F.);
#3644=ORIENTED_EDGE('',*,*,#2640,.T.);
#3645=ORIENTED_EDGE('',*,*,#2627,.T.);
#3646=ORIENTED_EDGE('',*,*,#2641,.T.);
#3647=ORIENTED_EDGE('',*,*,#2638,.F.);
#3648=ORIENTED_EDGE('',*,*,#2640,.F.);
#3649=ORIENTED_EDGE('',*,*,#2637,.F.);
#3650=ORIENTED_EDGE('',*,*,#2634,.F.);
#3651=ORIENTED_EDGE('',*,*,#2631,.F.);
#3652=ORIENTED_EDGE('',*,*,#2628,.F.);
#3653=ORIENTED_EDGE('',*,*,#2624,.F.);
#3654=ORIENTED_EDGE('',*,*,#2641,.F.);
#3655=ORIENTED_EDGE('',*,*,#2626,.F.);
#3656=ORIENTED_EDGE('',*,*,#2630,.F.);
#3657=ORIENTED_EDGE('',*,*,#2633,.F.);
#3658=ORIENTED_EDGE('',*,*,#2636,.F.);
#3659=ORIENTED_EDGE('',*,*,#2639,.F.);
#3736=CYLINDRICAL_SURFACE('',#4649,0.35);
#3737=CYLINDRICAL_SURFACE('',#4657,0.1954);
#3947=ADVANCED_FACE('',(#704),#484,.T.);
#3948=ADVANCED_FACE('',(#705),#177,.T.);
#3949=ADVANCED_FACE('',(#706),#3736,.T.);
#3950=ADVANCED_FACE('',(#707),#178,.T.);
#3951=ADVANCED_FACE('',(#708,#358),#485,.T.);
#3952=ADVANCED_FACE('',(#709),#179,.T.);
#3953=ADVANCED_FACE('',(#710),#3737,.T.);
#3954=ADVANCED_FACE('',(#711),#180,.T.);
#3955=ADVANCED_FACE('',(#712),#486,.T.);
#3956=ADVANCED_FACE('',(#713),#487,.F.);
#3957=ADVANCED_FACE('',(#714),#488,.F.);
#3958=ADVANCED_FACE('',(#715),#489,.F.);
#3959=ADVANCED_FACE('',(#716),#490,.F.);
#3960=ADVANCED_FACE('',(#717),#491,.F.);
#3961=ADVANCED_FACE('',(#718),#492,.F.);
#3962=ADVANCED_FACE('',(#719),#493,.F.);
#3963=ADVANCED_FACE('',(#720),#494,.F.);
#3984=CLOSED_SHELL('',(#3947,#3948,#3949,#3950,#3951,#3952,#3953,#3954,
#3955));
#3985=CLOSED_SHELL('',(#3956,#3957,#3958,#3959,#3960,#3961,#3962,#3963));
#4644=AXIS2_PLACEMENT_3D('',#7193,#5837,#5838);
#4645=AXIS2_PLACEMENT_3D('',#7194,#5839,#5840);
#4646=AXIS2_PLACEMENT_3D('',#7196,#5841,#5842);
#4647=AXIS2_PLACEMENT_3D('',#7197,#5843,#5844);
#4648=AXIS2_PLACEMENT_3D('',#7199,#5845,#5846);
#4649=AXIS2_PLACEMENT_3D('',#7201,#5848,#5849);
#4650=AXIS2_PLACEMENT_3D('',#7203,#5850,#5851);
#4651=AXIS2_PLACEMENT_3D('',#7205,#5853,#5854);
#4652=AXIS2_PLACEMENT_3D('',#7207,#5855,#5856);
#4653=AXIS2_PLACEMENT_3D('',#7209,#5858,#5859);
#4654=AXIS2_PLACEMENT_3D('',#7211,#5860,#5861);
#4655=AXIS2_PLACEMENT_3D('',#7212,#5862,#5863);
#4656=AXIS2_PLACEMENT_3D('',#7214,#5864,#5865);
#4657=AXIS2_PLACEMENT_3D('',#7216,#5867,#5868);
#4658=AXIS2_PLACEMENT_3D('',#7218,#5869,#5870);
#4659=AXIS2_PLACEMENT_3D('',#7220,#5872,#5873);
#4660=AXIS2_PLACEMENT_3D('',#7222,#5874,#5875);
#4661=AXIS2_PLACEMENT_3D('',#7224,#5877,#5878);
#4662=AXIS2_PLACEMENT_3D('',#7225,#5879,#5880);
#4663=AXIS2_PLACEMENT_3D('',#7234,#5885,#5886);
#4664=AXIS2_PLACEMENT_3D('',#7240,#5890,#5891);
#4665=AXIS2_PLACEMENT_3D('',#7246,#5895,#5896);
#4666=AXIS2_PLACEMENT_3D('',#7252,#5900,#5901);
#4667=AXIS2_PLACEMENT_3D('',#7258,#5905,#5906);
#4668=AXIS2_PLACEMENT_3D('',#7261,#5909,#5910);
#4669=AXIS2_PLACEMENT_3D('',#7262,#5911,#5912);
#5837=DIRECTION('axis',(0.,0.,1.));
#5838=DIRECTION('refdir',(1.,0.,0.));
#5839=DIRECTION('center_axis',(0.,1.,0.));
#5840=DIRECTION('ref_axis',(0.,0.,1.));
#5841=DIRECTION('center_axis',(0.,-1.,0.));
#5842=DIRECTION('ref_axis',(1.,0.,0.));
#5843=DIRECTION('center_axis',(0.,-1.,0.));
#5844=DIRECTION('ref_axis',(1.,0.,0.));
#5845=DIRECTION('center_axis',(0.,-1.,0.));
#5846=DIRECTION('ref_axis',(1.,0.,0.));
#5847=DIRECTION('',(0.707106781186547,0.707106781186548,8.65956056235493E-17));
#5848=DIRECTION('center_axis',(0.,-1.,0.));
#5849=DIRECTION('ref_axis',(1.,0.,0.));
#5850=DIRECTION('center_axis',(0.,-1.,0.));
#5851=DIRECTION('ref_axis',(1.,0.,0.));
#5852=DIRECTION('',(0.,1.,0.));
#5853=DIRECTION('center_axis',(0.,1.,0.));
#5854=DIRECTION('ref_axis',(1.,0.,0.));
#5855=DIRECTION('center_axis',(0.,-1.,0.));
#5856=DIRECTION('ref_axis',(1.,0.,0.));
#5857=DIRECTION('',(-0.707106781186547,0.707106781186548,-8.65956056235493E-17));
#5858=DIRECTION('center_axis',(0.,-1.,0.));
#5859=DIRECTION('ref_axis',(0.,0.,-1.));
#5860=DIRECTION('center_axis',(0.,-1.,0.));
#5861=DIRECTION('ref_axis',(1.,0.,0.));
#5862=DIRECTION('center_axis',(0.,1.,0.));
#5863=DIRECTION('ref_axis',(1.,0.,0.));
#5864=DIRECTION('center_axis',(0.,1.,0.));
#5865=DIRECTION('ref_axis',(1.,0.,0.));
#5866=DIRECTION('',(-0.447213595499958,0.894427190999916,-5.47678698264203E-17));
#5867=DIRECTION('center_axis',(0.,-1.,0.));
#5868=DIRECTION('ref_axis',(1.,0.,0.));
#5869=DIRECTION('center_axis',(0.,1.,0.));
#5870=DIRECTION('ref_axis',(1.,0.,0.));
#5871=DIRECTION('',(0.,1.,0.));
#5872=DIRECTION('center_axis',(0.,1.,0.));
#5873=DIRECTION('ref_axis',(1.,0.,0.));
#5874=DIRECTION('center_axis',(0.,-1.,0.));
#5875=DIRECTION('ref_axis',(1.,0.,0.));
#5876=DIRECTION('',(-0.707106781186547,0.707106781186548,-8.65956056235493E-17));
#5877=DIRECTION('center_axis',(0.,-1.,0.));
#5878=DIRECTION('ref_axis',(0.,0.,-1.));
#5879=DIRECTION('center_axis',(0.866025403784439,0.,-0.5));
#5880=DIRECTION('ref_axis',(0.5,0.,0.866025403784439));
#5881=DIRECTION('',(-0.5,0.,-0.866025403784439));
#5882=DIRECTION('',(0.,-1.,0.));
#5883=DIRECTION('',(0.5,0.,0.866025403784439));
#5884=DIRECTION('',(0.,-1.,0.));
#5885=DIRECTION('center_axis',(1.60246890531964E-16,0.,-1.));
#5886=DIRECTION('ref_axis',(1.,0.,1.60246890531964E-16));
#5887=DIRECTION('',(-1.,0.,-1.60246890531964E-16));
#5888=DIRECTION('',(0.,-1.,0.));
#5889=DIRECTION('',(1.,0.,1.60246890531964E-16));
#5890=DIRECTION('center_axis',(-0.866025403784439,0.,-0.5));
#5891=DIRECTION('ref_axis',(0.5,0.,-0.866025403784439));
#5892=DIRECTION('',(-0.5,0.,0.866025403784439));
#5893=DIRECTION('',(0.,-1.,0.));
#5894=DIRECTION('',(0.5,0.,-0.866025403784439));
#5895=DIRECTION('center_axis',(-0.866025403784439,0.,0.5));
#5896=DIRECTION('ref_axis',(-0.5,0.,-0.866025403784439));
#5897=DIRECTION('',(0.5,0.,0.866025403784439));
#5898=DIRECTION('',(0.,-1.,0.));
#5899=DIRECTION('',(-0.5,0.,-0.866025403784439));
#5900=DIRECTION('center_axis',(-1.60246890531964E-16,0.,1.));
#5901=DIRECTION('ref_axis',(-1.,0.,-1.60246890531964E-16));
#5902=DIRECTION('',(1.,0.,1.60246890531964E-16));
#5903=DIRECTION('',(0.,-1.,0.));
#5904=DIRECTION('',(-1.,0.,-1.60246890531964E-16));
#5905=DIRECTION('center_axis',(0.866025403784439,0.,0.5));
#5906=DIRECTION('ref_axis',(-0.5,0.,0.866025403784439));
#5907=DIRECTION('',(0.5,0.,-0.866025403784439));
#5908=DIRECTION('',(-0.5,0.,0.866025403784439));
#5909=DIRECTION('center_axis',(0.,1.,0.));
#5910=DIRECTION('ref_axis',(1.,0.,0.));
#5911=DIRECTION('center_axis',(0.,-1.,0.));
#5912=DIRECTION('ref_axis',(0.,0.,-1.));
#7193=CARTESIAN_POINT('',(0.,0.,0.));
#7194=CARTESIAN_POINT('Origin',(0.3,0.4,0.));
#7195=CARTESIAN_POINT('',(-0.3,0.4,-3.67394039744206E-17));
#7196=CARTESIAN_POINT('Origin',(0.,0.4,0.));
#7197=CARTESIAN_POINT('Origin',(0.,0.375,0.));
#7198=CARTESIAN_POINT('',(-0.35,0.35,-4.28626379701573E-17));
#7199=CARTESIAN_POINT('Origin',(0.,0.35,0.));
#7200=CARTESIAN_POINT('',(-0.325,0.375,-3.9801020972289E-17));
#7201=CARTESIAN_POINT('Origin',(0.,0.19,0.));
#7202=CARTESIAN_POINT('',(-0.35,0.03,-4.28626379701574E-17));
#7203=CARTESIAN_POINT('Origin',(0.,0.03,0.));
#7204=CARTESIAN_POINT('',(-0.35,0.19,-4.28626379701574E-17));
#7205=CARTESIAN_POINT('Origin',(0.,0.0149999999999999,0.));
#7206=CARTESIAN_POINT('',(-0.32,-3.29597460435593E-17,-3.91886975727153E-17));
#7207=CARTESIAN_POINT('Origin',(0.,0.,0.));
#7208=CARTESIAN_POINT('',(-0.335,0.0149999999999999,-4.10256677714363E-17));
#7209=CARTESIAN_POINT('Origin',(0.22,0.,0.));
#7210=CARTESIAN_POINT('',(-0.22,-6.93889390390723E-18,-2.69422295812418E-17));
#7211=CARTESIAN_POINT('Origin',(0.,0.,0.));
#7212=CARTESIAN_POINT('Origin',(0.,-0.02,0.));
#7213=CARTESIAN_POINT('',(-0.1954,-0.0492,2.39295984553393E-17));
#7214=CARTESIAN_POINT('Origin',(0.,-0.0492,0.));
#7215=CARTESIAN_POINT('',(-0.21,-0.02,-2.57175827820944E-17));
#7216=CARTESIAN_POINT('Origin',(0.,-0.8,0.));
#7217=CARTESIAN_POINT('',(-0.1954,-1.5646,2.39295984553393E-17));
#7218=CARTESIAN_POINT('Origin',(0.,-1.5646,0.));
#7219=CARTESIAN_POINT('',(-0.1954,-0.8,-2.39295984553393E-17));
#7220=CARTESIAN_POINT('Origin',(0.,-1.58,0.));
#7221=CARTESIAN_POINT('',(-0.16,-1.6,-1.95943487863577E-17));
#7222=CARTESIAN_POINT('Origin',(0.,-1.6,0.));
#7223=CARTESIAN_POINT('',(-0.18,-1.58,-2.20436423846524E-17));
#7224=CARTESIAN_POINT('Origin',(0.,-1.6,0.));
#7225=CARTESIAN_POINT('Origin',(0.0866025403784439,-0.4,-0.15));
#7226=CARTESIAN_POINT('',(0.173205080756888,-0.4,0.));
#7227=CARTESIAN_POINT('',(0.0866025403784439,-0.4,-0.15));
#7228=CARTESIAN_POINT('',(0.173205080756888,-0.4,0.));
#7229=CARTESIAN_POINT('',(0.0866025403784439,-0.64,-0.15));
#7230=CARTESIAN_POINT('',(0.0866025403784439,-0.4,-0.15));
#7231=CARTESIAN_POINT('',(0.173205080756888,-0.64,0.));
#7232=CARTESIAN_POINT('',(0.173205080756888,-0.64,0.));
#7233=CARTESIAN_POINT('',(0.173205080756888,-0.4,0.));
#7234=CARTESIAN_POINT('Origin',(-0.0866025403784438,-0.4,-0.15));
#7235=CARTESIAN_POINT('',(-0.0866025403784438,-0.4,-0.15));
#7236=CARTESIAN_POINT('',(0.0866025403784439,-0.4,-0.15));
#7237=CARTESIAN_POINT('',(-0.0866025403784438,-0.64,-0.15));
#7238=CARTESIAN_POINT('',(-0.0866025403784438,-0.4,-0.15));
#7239=CARTESIAN_POINT('',(0.0866025403784439,-0.64,-0.15));
#7240=CARTESIAN_POINT('Origin',(-0.173205080756888,-0.4,-2.77555756156289E-17));
#7241=CARTESIAN_POINT('',(-0.173205080756888,-0.4,-2.12115047744981E-17));
#7242=CARTESIAN_POINT('',(-0.0866025403784438,-0.4,-0.15));
#7243=CARTESIAN_POINT('',(-0.173205080756888,-0.64,-2.77555756156289E-17));
#7244=CARTESIAN_POINT('',(-0.173205080756888,-0.4,-2.12115047744981E-17));
#7245=CARTESIAN_POINT('',(-0.0866025403784438,-0.64,-0.15));
#7246=CARTESIAN_POINT('Origin',(-0.0866025403784439,-0.4,0.15));
#7247=CARTESIAN_POINT('',(-0.0866025403784439,-0.4,0.15));
#7248=CARTESIAN_POINT('',(-0.173205080756888,-0.4,-2.12115047744981E-17));
#7249=CARTESIAN_POINT('',(-0.0866025403784439,-0.64,0.15));
#7250=CARTESIAN_POINT('',(-0.0866025403784439,-0.4,0.15));
#7251=CARTESIAN_POINT('',(-0.173205080756888,-0.64,-2.12115047744981E-17));
#7252=CARTESIAN_POINT('Origin',(0.0866025403784439,-0.4,0.15));
#7253=CARTESIAN_POINT('',(0.0866025403784439,-0.4,0.15));
#7254=CARTESIAN_POINT('',(-0.0866025403784439,-0.4,0.15));
#7255=CARTESIAN_POINT('',(0.0866025403784439,-0.64,0.15));
#7256=CARTESIAN_POINT('',(0.0866025403784439,-0.4,0.15));
#7257=CARTESIAN_POINT('',(-0.0866025403784439,-0.64,0.15));
#7258=CARTESIAN_POINT('Origin',(0.173205080756888,-0.4,0.));
#7259=CARTESIAN_POINT('',(0.0866025403784439,-0.4,0.15));
#7260=CARTESIAN_POINT('',(0.0866025403784439,-0.64,0.15));
#7261=CARTESIAN_POINT('Origin',(0.,-0.4,-2.77555756156289E-17));
#7262=CARTESIAN_POINT('Origin',(0.,-0.64,-2.77555756156289E-17));
#7323=UNCERTAINTY_MEASURE_WITH_UNIT(LENGTH_MEASURE(0.001),#7350,
'DISTANCE_ACCURACY_VALUE',
'Maximum model space distance between geometric entities at asserted c
onnectivities');
#7324=UNCERTAINTY_MEASURE_WITH_UNIT(LENGTH_MEASURE(0.001),#7350,
'DISTANCE_ACCURACY_VALUE',
'Maximum model space distance between geometric entities at asserted c
onnectivities');
#7348=(
GEOMETRIC_REPRESENTATION_CONTEXT(3)
GLOBAL_UNCERTAINTY_ASSIGNED_CONTEXT((#7323))
GLOBAL_UNIT_ASSIGNED_CONTEXT((#7350,#7352,#7353))
REPRESENTATION_CONTEXT('','3D')
);
#7349=(
GEOMETRIC_REPRESENTATION_CONTEXT(3)
GLOBAL_UNCERTAINTY_ASSIGNED_CONTEXT((#7324))
GLOBAL_UNIT_ASSIGNED_CONTEXT((#7350,#7352,#7353))
REPRESENTATION_CONTEXT('','3D')
);
#7350=(
LENGTH_UNIT()
NAMED_UNIT(*)
SI_UNIT(.CENTI.,.METRE.)
);
#7352=(
NAMED_UNIT(*)
PLANE_ANGLE_UNIT()
SI_UNIT($,.RADIAN.)
);
#7353=(
NAMED_UNIT(*)
SI_UNIT($,.STERADIAN.)
SOLID_ANGLE_UNIT()
);
#7377=SHAPE_DEFINITION_REPRESENTATION(#7403,#7464);
#7403=PRODUCT_DEFINITION_SHAPE('',$,#7489);
#7464=SHAPE_REPRESENTATION('',(#4644),#7348);
#7465=PRODUCT_DEFINITION_CONTEXT('part definition',#7539,'design');
#7489=PRODUCT_DEFINITION('Cap Screw - M4x16','Cap Screw - M4x16',#7513,
#7465);
#7513=PRODUCT_DEFINITION_FORMATION('',$,#7564);
#7539=APPLICATION_CONTEXT(
'Core Data for Automotive Mechanical Design Process');
#7540=PRODUCT_CONTEXT('part definition',#7539,'mechanical');
#7564=PRODUCT('Cap Screw - M4x16','Cap Screw - M4x16',
'Cap Screw - M4x16',(#7540));
#7628=COLOUR_RGB('Black',0.12,0.14,0.17);
#7629=FILL_AREA_STYLE_COLOUR('',#7628);
#7630=FILL_AREA_STYLE('',(#7629));
#7631=SURFACE_STYLE_FILL_AREA(#7630);
#7632=SURFACE_SIDE_STYLE('',(#7631));
#7633=SURFACE_STYLE_USAGE(.BOTH.,#7632);
#7634=PRESENTATION_STYLE_ASSIGNMENT((#7633));
ENDSEC;
END-ISO-10303-21;
